ISO-10303-21;
HEADER;
FILE_DESCRIPTION (('STEP AP214'),
    '1' );
FILE_NAME ('Socket Head Cap Screw L.step',
    '2026-10-09T10:51:02',
    ( '' ),
    ( '' ),
    'SwSTEP 2.0',
    'SolidWorks 2026',
    '' );
FILE_SCHEMA (( 'AUTOMOTIVE_DESIGN' ));
ENDSEC;

DATA;
#46=ADVANCED_BREP_SHAPE_REPRESENTATION ( '', ( #9964, #6292 ), #9601 ) ;
#69=VECTOR ( 'NONE', #9378, 999.9999999999998863 ) ;
#122=FACE_OUTER_BOUND ( 'NONE', #5169, .T. ) ;
#135=ORIENTED_EDGE ( 'NONE', *, *, #14584, .T. ) ;
#174=AXIS2_PLACEMENT_3D ( 'NONE', #13516, #3386, #10402 ) ;
#291=DIRECTION ( 'NONE',  ( 7.125109674160258889E-05, -0.9999848031710252272, 0.005512562950849897447 ) ) ;
#307=VERTEX_POINT ( 'NONE', #5575 ) ;
#351=CIRCLE ( 'NONE', #15405, 6.500000000000013323 ) ;
#362=EDGE_LOOP ( 'NONE', ( #12674, #9127, #10341, #20941, #20495 ) ) ;
#381=DIRECTION ( 'NONE',  ( 7.125109674160258889E-05, -0.9999848031710252272, 0.005512562950849897447 ) ) ;
#410=PLANE ( 'NONE',  #2962 ) ;
#418=CIRCLE ( 'NONE', #14381, 0.3999999999999986899 ) ;
#441=ORIENTED_EDGE ( 'NONE', *, *, #16971, .F. ) ;
#456=CARTESIAN_POINT ( 'NONE',  ( -9.065023647928146744, 109.7167603697149474, 130.3064260814875013 ) ) ;
#458=ORIENTED_EDGE ( 'NONE', *, *, #12740, .T. ) ;
#523=( NAMED_UNIT ( * ) PLANE_ANGLE_UNIT ( ) SI_UNIT ( $, .RADIAN. ) );
#543=DIRECTION ( 'NONE',  ( -0.01035335185279156155, -0.005513005182357613894, -0.9999312050732649393 ) ) ;
#549=LINE ( 'NONE', #12727, #2646 ) ;
#555=VERTEX_POINT ( 'NONE', #13234 ) ;
#581=ORIENTED_EDGE ( 'NONE', *, *, #18788, .F. ) ;
#592=VERTEX_POINT ( 'NONE', #4683 ) ;
#593=DIRECTION ( 'NONE',  ( -7.125109674160258889E-05, 0.9999848031710252272, -0.005512562950849897447 ) ) ;
#597=LINE ( 'NONE', #15896, #8146 ) ;
#612=EDGE_CURVE ( 'NONE', #15083, #18866, #14842, .T. ) ;
#633=DIRECTION ( 'NONE',  ( 0.01035335185279153900, 0.005513005182355262476, 0.9999312050732647172 ) ) ;
#651=CARTESIAN_POINT ( 'NONE',  ( -10.81485622274934677, 114.1219197046086009, 131.2528221548242584 ) ) ;
#717=TOROIDAL_SURFACE ( 'NONE', #21293, 4.400000000000000355, 0.4000000000000000222 ) ;
#720=CARTESIAN_POINT ( 'NONE',  ( -10.81834107826543168, 163.0306764353018991, 130.9832054571796789 ) ) ;
#725=CARTESIAN_POINT ( 'NONE',  ( -10.85567112094788200, 105.6999953372425551, 127.2994028633183348 ) ) ;
#792=DIRECTION ( 'NONE',  ( 7.125109674160258889E-05, -0.9999848031710253382, 0.005512562950849898315 ) ) ;
#938=SHAPE_REPRESENTATION ( 'Socket Head Cap Screw L', ( #6292 ), #9601 ) ;
#970=ORIENTED_EDGE ( 'NONE', *, *, #22626, .T. ) ;
#1000=CARTESIAN_POINT ( 'NONE',  ( -10.82440428556346568, 109.7167354332198812, 130.3246429589756872 ) ) ;
#1006=CARTESIAN_POINT ( 'NONE',  ( -9.128127327470902941, 109.6831586031284758, 124.2118453865659546 ) ) ;
#1030=FACE_OUTER_BOUND ( 'NONE', #15887, .T. ) ;
#1039=ORIENTED_EDGE ( 'NONE', *, *, #20033, .T. ) ;
#1056=DIRECTION ( 'NONE',  ( 7.125109674160258889E-05, -0.9999848031710252272, 0.005512562950849897447 ) ) ;
#1135=VECTOR ( 'NONE', #13086, 999.9999999999998863 ) ;
#1159=ORIENTED_EDGE ( 'NONE', *, *, #9526, .T. ) ;
#1166=EDGE_LOOP ( 'NONE', ( #9714, #12873, #7358 ) ) ;
#1167=CIRCLE ( 'NONE', #19113, 4.000000000000006217 ) ;
#1218=CIRCLE ( 'NONE', #19175, 3.309500000000006992 ) ;
#1244=EDGE_CURVE ( 'NONE', #1880, #592, #5018, .T. ) ;
#1345=PLANE ( 'NONE',  #174 ) ;
#1385=EDGE_LOOP ( 'NONE', ( #12013, #19855, #11519, #22409, #1884 ) ) ;
#1395=DIRECTION ( 'NONE',  ( 1.000000000000000000, 0.000000000000000000, 0.000000000000000000 ) ) ;
#1402=CARTESIAN_POINT ( 'NONE',  ( -10.81199549121517123, 73.97252985729198826, 131.4741515573008712 ) ) ;
#1445=VECTOR ( 'NONE', #6783, 1000.000000000000114 ) ;
#1455=AXIS2_PLACEMENT_3D ( 'NONE', #6045, #2481, #18131 ) ;
#1483=APPLICATION_CONTEXT ( 'automotive_design' ) ;
#1537=DIRECTION ( 'NONE',  ( 0.9999464000778710560, 1.417269118681125921E-05, -0.01035358732233959689 ) ) ;
#1568=ADVANCED_FACE ( 'NONE', ( #5152 ), #15756, .T. ) ;
#1589=ORIENTED_EDGE ( 'NONE', *, *, #17013, .T. ) ;
#1636=CARTESIAN_POINT ( 'NONE',  ( -12.58378492319879527, 109.7167104967248434, 130.3428598364639299 ) ) ;
#1705=CARTESIAN_POINT ( 'NONE',  ( -12.64660359835458792, 105.6831695174542745, 124.2703293933457758 ) ) ;
#1790=ORIENTED_EDGE ( 'NONE', *, *, #20218, .F. ) ;
#1833=DIRECTION ( 'NONE',  ( 7.125109674160258889E-05, -0.9999848031710252272, 0.005512562950849896580 ) ) ;
#1839=( NAMED_UNIT ( * ) PLANE_ANGLE_UNIT ( ) SI_UNIT ( $, .RADIAN. ) );
#1880=VERTEX_POINT ( 'NONE', #19357 ) ;
#1884=ORIENTED_EDGE ( 'NONE', *, *, #11653, .T. ) ;
#1907=ADVANCED_FACE ( 'NONE', ( #3621 ), #22276, .F. ) ;
#1923=AXIS2_PLACEMENT_3D ( 'NONE', #18598, #18929, #6322 ) ;
#2002=DIRECTION ( 'NONE',  ( -0.01035335185279151644, -0.005513005182356664133, -0.9999312050732649393 ) ) ;
#2026=MECHANICAL_DESIGN_GEOMETRIC_PRESENTATION_REPRESENTATION('',(#3118),#7538);
#2086=DIRECTION ( 'NONE',  ( 0.01035335185279032469, 0.005513005182356926943, 0.9999312050732648283 ) ) ;
#2121=CARTESIAN_POINT ( 'NONE',  ( -10.85980368455889433, 163.6991139211620236, 126.9796742121690443 ) ) ;
#2140=CARTESIAN_POINT ( 'NONE',  ( -14.37471740060550118, 109.6998846769365628, 127.3137863664913425 ) ) ;
#2147=CARTESIAN_POINT ( 'NONE',  ( -10.85595612533484911, 109.6999345499266525, 127.2773526115149281 ) ) ;
#2178=CARTESIAN_POINT ( 'NONE',  ( -10.85572812182527613, 106.4999831797793775, 127.2949928129576733 ) ) ;
#2199=EDGE_CURVE ( 'NONE', #18866, #17838, #20635, .T. ) ;
#2233=AXIS2_PLACEMENT_3D ( 'NONE', #5351, #5587, #7431 ) ;
#2237=ORIENTED_EDGE ( 'NONE', *, *, #8286, .F. ) ;
#2269=CARTESIAN_POINT ( 'NONE',  ( -12.58349991881183172, 105.7167712840407319, 130.3649100882673224 ) ) ;
#2354=DIRECTION ( 'NONE',  ( 0.01035335185279151644, 0.005513005182356664133, 0.9999312050732649393 ) ) ;
#2399=DIRECTION ( 'NONE',  ( 7.125109674160258889E-05, -0.9999848031710252272, 0.005512562950849896580 ) ) ;
#2424=EDGE_CURVE ( 'NONE', #15988, #5453, #7133, .T. ) ;
#2447=ORIENTED_EDGE ( 'NONE', *, *, #1244, .T. ) ;
#2457=FACE_OUTER_BOUND ( 'NONE', #21949, .T. ) ;
#2467=ORIENTED_EDGE ( 'NONE', *, *, #19157, .F. ) ;
#2481=DIRECTION ( 'NONE',  ( 7.125109674160258889E-05, -0.9999848031710252272, 0.005512562950849897447 ) ) ;
#2539=FACE_OUTER_BOUND ( 'NONE', #362, .T. ) ;
#2542=ORIENTED_EDGE ( 'NONE', *, *, #17136, .F. ) ;
#2550=EDGE_CURVE ( 'NONE', #17838, #307, #351, .T. ) ;
#2580=VECTOR ( 'NONE', #3755, 1000.000000000000000 ) ;
#2646=VECTOR ( 'NONE', #17799, 1000.000000000000114 ) ;
#2675=CARTESIAN_POINT ( 'NONE',  ( -10.85340889862633595, 73.95047783656255547, 127.4744267370078177 ) ) ;
#2693=DIRECTION ( 'NONE',  ( 7.125109674160258889E-05, -0.9999848031710252272, 0.005512562950849896580 ) ) ;
#2760=EDGE_CURVE ( 'NONE', #307, #17838, #21944, .T. ) ;
#2762=DIRECTION ( 'NONE',  ( -0.01035335185279159971, -0.005513005182356926943, -0.9999312050732648283 ) ) ;
#2799=LINE ( 'NONE', #6575, #13371 ) ;
#2878=DIRECTION ( 'NONE',  ( 0.4910069343201003411, -0.004767316193522950878, -0.8711426192914037969 ) ) ;
#2904=ORIENTED_EDGE ( 'NONE', *, *, #21545, .T. ) ;
#2912=EDGE_CURVE ( 'NONE', #4443, #18526, #12890, .T. ) ;
#2962=AXIS2_PLACEMENT_3D ( 'NONE', #19575, #3850, #5332 ) ;
#2981=AXIS2_PLACEMENT_3D ( 'NONE', #1636, #15550, #15221 ) ;
#3009=ORIENTED_EDGE ( 'NONE', *, *, #20733, .T. ) ;
#3017=EDGE_CURVE ( 'NONE', #555, #4443, #6639, .T. ) ;
#3025=ADVANCED_FACE ( 'NONE', ( #21100 ), #10886, .T. ) ;
#3026=EDGE_CURVE ( 'NONE', #10108, #11275, #11366, .T. ) ;
#3043=ADVANCED_FACE ( 'NONE', ( #13999 ), #21605, .T. ) ;
#3096=FACE_OUTER_BOUND ( 'NONE', #16126, .T. ) ;
#3102=CARTESIAN_POINT ( 'NONE',  ( 0.000000000000000000, 0.000000000000000000, 0.000000000000000000 ) ) ;
#3118=STYLED_ITEM ( 'NONE', ( #21133 ), #9964 ) ;
#3208=FILL_AREA_STYLE_COLOUR ( '', #4212 ) ;
#3332=( NAMED_UNIT ( * ) SI_UNIT ( $, .STERADIAN. ) SOLID_ANGLE_UNIT ( ) );
#3386=DIRECTION ( 'NONE',  ( -0.8608023089638389136, 0.002744228680570687078, 0.5089320721780778989 ) ) ;
#3465=DIRECTION ( 'NONE',  ( 7.125109674160258889E-05, -0.9999848031710252272, 0.005512562950849897447 ) ) ;
#3478=AXIS2_PLACEMENT_3D ( 'NONE', #22465, #18496, #15402 ) ;
#3528=CARTESIAN_POINT ( 'NONE',  ( -12.58378492319879527, 109.7167104967248434, 130.3428598364639299 ) ) ;
#3532=DIRECTION ( 'NONE',  ( 0.01035335185279138807, 0.005513005182356417802, 0.9999312050732649393 ) ) ;
#3543=DIRECTION ( 'NONE',  ( 7.125109674160258889E-05, -0.9999848031710252272, 0.005512562950849897447 ) ) ;
#3557=SURFACE_STYLE_FILL_AREA ( #19293 ) ;
#3599=CARTESIAN_POINT ( 'NONE',  ( -14.37471740060550118, 109.6998846769365628, 127.3137863664913425 ) ) ;
#3621=FACE_OUTER_BOUND ( 'NONE', #7261, .T. ) ;
#3630=CARTESIAN_POINT ( 'NONE',  ( -10.79665701538697320, 105.7314194667820004, 132.9990107322359449 ) ) ;
#3648=ADVANCED_FACE ( 'NONE', ( #9684 ), #17559, .T. ) ;
#3731=ORIENTED_EDGE ( 'NONE', *, *, #5044, .F. ) ;
#3732=AXIS2_PLACEMENT_3D ( 'NONE', #8705, #12652, #21233 ) ;
#3736=AXIS2_PLACEMENT_3D ( 'NONE', #11014, #5614, #12859 ) ;
#3755=DIRECTION ( 'NONE',  ( 0.007270543169446074330, 0.7109943187548881660, 0.7031601651830782229 ) ) ;
#3764=AXIS2_PLACEMENT_3D ( 'NONE', #8596, #13682, #22251 ) ;
#3801=ORIENTED_EDGE ( 'NONE', *, *, #16971, .T. ) ;
#3850=DIRECTION ( 'NONE',  ( -7.125109674160258889E-05, 0.9999848031710252272, -0.005512562950849896580 ) ) ;
#3933=CARTESIAN_POINT ( 'NONE',  ( -10.82553926660208354, 163.7173592118130045, 130.2889465353590310 ) ) ;
#3946=EDGE_LOOP ( 'NONE', ( #5781, #16810, #11865, #8078 ) ) ;
#4098=FACE_OUTER_BOUND ( 'NONE', #10798, .T. ) ;
#4106=DIRECTION ( 'NONE',  ( 0.4910069343201003411, -0.004767316193522950878, -0.8711426192914037969 ) ) ;
#4179=CARTESIAN_POINT ( 'NONE',  ( -10.85595612533484911, 109.6999345499266525, 127.2773526115149281 ) ) ;
#4212=COLOUR_RGB ( '', 0.72549020, 0.75294118, 0.79215686) ;
#4225=LINE ( 'NONE', #11478, #10713 ) ;
#4241=ORIENTED_EDGE ( 'NONE', *, *, #18050, .T. ) ;
#4318=EDGE_CURVE ( 'NONE', #8712, #17192, #11639, .T. ) ;
#4341=VECTOR ( 'NONE', #17635, 1000.000000000000114 ) ;
#4391=FACE_OUTER_BOUND ( 'NONE', #12140, .T. ) ;
#4393=SHAPE_REPRESENTATION_RELATIONSHIP ( 'NONE' , 'NONE' ,  #938, #46 ) ;
#4436=CIRCLE ( 'NONE', #20205, 4.000000000000006217 ) ;
#4443=VERTEX_POINT ( 'NONE', #21064 ) ;
#4449=EDGE_CURVE ( 'NONE', #19436, #15988, #10851, .T. ) ;
#4451=ORIENTED_EDGE ( 'NONE', *, *, #12740, .F. ) ;
#4513=EDGE_LOOP ( 'NONE', ( #15106, #1039, #20699 ) ) ;
#4563=DIRECTION ( 'NONE',  ( 7.125109674160258889E-05, -0.9999848031710253382, 0.005512562950849898315 ) ) ;
#4576=ADVANCED_FACE ( 'NONE', ( #9771 ), #717, .F. ) ;
#4645=DIRECTION ( 'NONE',  ( -0.5089394657577703818, -0.004781488884709769391, -0.8607890319690654213 ) ) ;
#4650=CARTESIAN_POINT ( 'NONE',  ( -14.37443239621853408, 105.6999454642524654, 127.3358366182947634 ) ) ;
#4683=CARTESIAN_POINT ( 'NONE',  ( -10.79665701538697320, 105.7314194667820004, 132.9990107322359449 ) ) ;
#4755=ORIENTED_EDGE ( 'NONE', *, *, #17100, .F. ) ;
#4837=DIRECTION ( 'NONE',  ( -0.9999464000778708339, -1.417269118681738834E-05, 0.01035358732233848493 ) ) ;
#4900=ORIENTED_EDGE ( 'NONE', *, *, #2760, .T. ) ;
#4908=CARTESIAN_POINT ( 'NONE',  ( -12.64688860274155324, 109.6831087301383860, 124.2482791415423691 ) ) ;
#4945=CARTESIAN_POINT ( 'NONE',  ( -9.065023647928146744, 109.7167603697149474, 130.3064260814875013 ) ) ;
#4966=ORIENTED_EDGE ( 'NONE', *, *, #14712, .T. ) ;
#4970=EDGE_CURVE ( 'NONE', #19436, #7332, #18010, .T. ) ;
#5018=CIRCLE ( 'NONE', #20060, 5.699999999999990408 ) ;
#5019=PLANE ( 'NONE',  #3478 ) ;
#5027=CARTESIAN_POINT ( 'NONE',  ( -10.81071488200823083, 114.1241249066815442, 131.6527946368535709 ) ) ;
#5044=EDGE_CURVE ( 'NONE', #11676, #10601, #8045, .T. ) ;
#5054=DIRECTION ( 'NONE',  ( -0.4910069343201003411, 0.004767316193522951745, 0.8711426192914037969 ) ) ;
#5065=DIRECTION ( 'NONE',  ( -0.01035335185279151644, -0.005513005182356664133, -0.9999312050732649393 ) ) ;
#5089=CARTESIAN_POINT ( 'NONE',  ( -12.64688860274155324, 109.6831087301383860, 124.2482791415423691 ) ) ;
#5091=VERTEX_POINT ( 'NONE', #651 ) ;
#5094=EDGE_CURVE ( 'NONE', #13282, #10108, #9137, .T. ) ;
#5124=DIRECTION ( 'NONE',  ( -0.01035335185279127358, -0.005513005182357338940, -0.9999312050732649393 ) ) ;
#5152=FACE_OUTER_BOUND ( 'NONE', #1166, .T. ) ;
#5156=( LENGTH_UNIT ( ) NAMED_UNIT ( * ) SI_UNIT ( .MILLI., .METRE. ) );
#5169=EDGE_LOOP ( 'NONE', ( #12023, #15573, #11662, #7611, #21887 ) ) ;
#5187=FACE_OUTER_BOUND ( 'NONE', #1385, .T. ) ;
#5194=ORIENTED_EDGE ( 'NONE', *, *, #12186, .T. ) ;
#5225=DIRECTION ( 'NONE',  ( 7.125109674160258889E-05, -0.9999848031710253382, 0.005512562950849898315 ) ) ;
#5278=ORIENTED_EDGE ( 'NONE', *, *, #14712, .F. ) ;
#5288=CARTESIAN_POINT ( 'NONE',  ( -13.51080300167352810, 109.6914967035374673, 125.7810327540168629 ) ) ;
#5310=AXIS2_PLACEMENT_3D ( 'NONE', #2675, #1056, #8047 ) ;
#5329=( LENGTH_UNIT ( ) NAMED_UNIT ( * ) SI_UNIT ( .MILLI., .METRE. ) );
#5332=DIRECTION ( 'NONE',  ( -0.01035335185279143318, -0.005513005182356926943, -0.9999312050732649393 ) ) ;
#5351=CARTESIAN_POINT ( 'NONE',  ( -10.85595612533484911, 109.6999345499266525, 127.2773526115149281 ) ) ;
#5352=ORIENTED_EDGE ( 'NONE', *, *, #612, .F. ) ;
#5415=CARTESIAN_POINT ( 'NONE',  ( -10.85340889862633595, 73.95047783656255547, 127.4744267370078177 ) ) ;
#5453=VERTEX_POINT ( 'NONE', #17357 ) ;
#5456=DIRECTION ( 'NONE',  ( -0.01035335185279156155, -0.005513005182357613894, -0.9999312050732649393 ) ) ;
#5459=VECTOR ( 'NONE', #6981, 1000.000000000000227 ) ;
#5551=EDGE_CURVE ( 'NONE', #9612, #10108, #7569, .T. ) ;
#5575=CARTESIAN_POINT ( 'NONE',  ( -10.78843133478213190, 106.5358177134646951, 133.7945456459338516 ) ) ;
#5587=DIRECTION ( 'NONE',  ( 7.125109674160258889E-05, -0.9999848031710252272, 0.005512562950849897447 ) ) ;
#5614=DIRECTION ( 'NONE',  ( 7.125109674160258889E-05, -0.9999848031710252272, 0.005512562950849896580 ) ) ;
#5650=VECTOR ( 'NONE', #4645, 1000.000000000000000 ) ;
#5673=EDGE_LOOP ( 'NONE', ( #19325, #12436, #20264 ) ) ;
#5698=DIRECTION ( 'NONE',  ( 7.125109674160258889E-05, -0.9999848031710252272, 0.005512562950849896580 ) ) ;
#5759=VERTEX_POINT ( 'NONE', #9974 ) ;
#5781=ORIENTED_EDGE ( 'NONE', *, *, #2199, .F. ) ;
#5792=AXIS2_PLACEMENT_3D ( 'NONE', #14456, #14218, #19470 ) ;
#5800=CARTESIAN_POINT ( 'NONE',  ( -14.37443239621853408, 105.6999454642524654, 127.3358366182947634 ) ) ;
#5862=ORIENTED_EDGE ( 'NONE', *, *, #12004, .T. ) ;
#5883=EDGE_CURVE ( 'NONE', #592, #307, #14345, .T. ) ;
#5903=CARTESIAN_POINT ( 'NONE',  ( -10.90179587787409865, 113.6756165398083880, 122.8556050573891838 ) ) ;
#5987=CARTESIAN_POINT ( 'NONE',  ( -10.91468522650879258, 105.6685712077031241, 121.5997949944007246 ) ) ;
#5998=ORIENTED_EDGE ( 'NONE', *, *, #5551, .T. ) ;
#6008=ORIENTED_EDGE ( 'NONE', *, *, #2760, .F. ) ;
#6045=CARTESIAN_POINT ( 'NONE',  ( -10.85595612533484911, 109.6999345499266525, 127.2773526115149281 ) ) ;
#6078=ORIENTED_EDGE ( 'NONE', *, *, #17151, .F. ) ;
#6098=DIRECTION ( 'NONE',  ( -0.007371307436792093500, 0.7031977520565657613, -0.7109561064716055645 ) ) ;
#6281=ADVANCED_FACE ( 'NONE', ( #4391 ), #14663, .T. ) ;
#6289=ORIENTED_EDGE ( 'NONE', *, *, #8066, .F. ) ;
#6291=CONICAL_SURFACE ( 'NONE', #8124, 3.309500000000006992, 0.7853981633974710386 ) ;
#6292=AXIS2_PLACEMENT_3D ( 'NONE', #3102, #12069, #1395 ) ;
#6299=DIRECTION ( 'NONE',  ( 0.007371307436792259166, -0.7031977520565497741, 0.7109561064716214407 ) ) ;
#6322=DIRECTION ( 'NONE',  ( 0.01035335185279115042, 0.005513005182354825326, 0.9999312050732648283 ) ) ;
#6390=CARTESIAN_POINT ( 'NONE',  ( -8.232661088767551760, 109.6915715130226232, 125.7263821215522341 ) ) ;
#6481=DIRECTION ( 'NONE',  ( -7.125109674160258889E-05, 0.9999848031710252272, -0.005512562950849897447 ) ) ;
#6532=DIRECTION ( 'NONE',  ( 0.01035335185279134471, 0.005513005182356394383, 0.9999312050732649393 ) ) ;
#6539=CARTESIAN_POINT ( 'NONE',  ( -10.85624112972181621, 113.6998737626107641, 127.2553023597115498 ) ) ;
#6550=DIRECTION ( 'NONE',  ( 7.125109674160258889E-05, -0.9999848031710253382, 0.005512562950849898315 ) ) ;
#6575=CARTESIAN_POINT ( 'NONE',  ( -9.065023647928146744, 109.7167603697149474, 130.3064260814875013 ) ) ;
#6639=LINE ( 'NONE', #4908, #12834 ) ;
#6701=DIRECTION ( 'NONE',  ( -0.8711556608166292071, -0.002768776501786239866, -0.4909991328951868184 ) ) ;
#6737=DIRECTION ( 'NONE',  ( 0.01035335185279115042, 0.005513005182354825326, 0.9999312050732648283 ) ) ;
#6740=EDGE_CURVE ( 'NONE', #592, #1880, #19117, .T. ) ;
#6783=DIRECTION ( 'NONE',  ( 0.5089394657577702707, 0.004781488884709769391, 0.8607890319690654213 ) ) ;
#6790=DIRECTION ( 'NONE',  ( -0.8711556608166292071, -0.002768776501786239432, -0.4909991328951867628 ) ) ;
#6806=LINE ( 'NONE', #13831, #14128 ) ;
#6968=ORIENTED_EDGE ( 'NONE', *, *, #5883, .T. ) ;
#6981=DIRECTION ( 'NONE',  ( 0.9999464000778708339, 1.417269118681874529E-05, -0.01035358732233823860 ) ) ;
#7021=AXIS2_PLACEMENT_3D ( 'NONE', #10098, #20646, #11938 ) ;
#7029=ORIENTED_EDGE ( 'NONE', *, *, #17100, .T. ) ;
#7065=FACE_OUTER_BOUND ( 'NONE', #10869, .T. ) ;
#7133=LINE ( 'NONE', #8499, #1445 ) ;
#7137=VERTEX_POINT ( 'NONE', #3933 ) ;
#7143=CARTESIAN_POINT ( 'NONE',  ( -10.78611211158319350, 73.98631237024787310, 133.9739795699840386 ) ) ;
#7188=LINE ( 'NONE', #12022, #18027 ) ;
#7192=CARTESIAN_POINT ( 'NONE',  ( -14.37471740060550118, 109.6998846769365628, 127.3137863664913425 ) ) ;
#7261=EDGE_LOOP ( 'NONE', ( #6078, #1589, #20520, #20162, #22145 ) ) ;
#7304=ADVANCED_FACE ( 'NONE', ( #11638, #22176 ), #11295, .T. ) ;
#7309=DIRECTION ( 'NONE',  ( 0.01035335185279143318, 0.005513005182356926943, 0.9999312050732649393 ) ) ;
#7322=AXIS2_PLACEMENT_3D ( 'NONE', #20986, #19602, #5124 ) ;
#7332=VERTEX_POINT ( 'NONE', #5288 ) ;
#7358=ORIENTED_EDGE ( 'NONE', *, *, #4970, .T. ) ;
#7381=CIRCLE ( 'NONE', #10686, 3.047499999999988329 ) ;
#7431=DIRECTION ( 'NONE',  ( 0.01035335185279153900, 0.005513005182355262476, 0.9999312050732647172 ) ) ;
#7481=PLANE ( 'NONE',  #18905 ) ;
#7538=( GEOMETRIC_REPRESENTATION_CONTEXT ( 3 ) GLOBAL_UNCERTAINTY_ASSIGNED_CONTEXT ( ( #16680 ) ) GLOBAL_UNIT_ASSIGNED_CONTEXT ( ( #5156, #1839, #3332 ) ) REPRESENTATION_CONTEXT ( 'NONE', 'WORKASPACE' ) );
#7569=LINE ( 'NONE', #456, #21977 ) ;
#7596=DIRECTION ( 'NONE',  ( 0.01035335185279129787, 0.005513005182357351951, 0.9999312050732647172 ) ) ;
#7611=ORIENTED_EDGE ( 'NONE', *, *, #3017, .F. ) ;
#7643=DIRECTION ( 'NONE',  ( 0.4910069343201003411, -0.004767316193522950878, -0.8711426192914036859 ) ) ;
#7659=EDGE_CURVE ( 'NONE', #5759, #22007, #597, .T. ) ;
#7721=DIRECTION ( 'NONE',  ( -7.125109674160258889E-05, 0.9999848031710252272, -0.005512562950849897447 ) ) ;
#7843=EDGE_CURVE ( 'NONE', #5091, #11676, #8884, .T. ) ;
#7866=CARTESIAN_POINT ( 'NONE',  ( -9.065023647928146744, 109.7167603697149474, 130.3064260814875013 ) ) ;
#7893=ADVANCED_FACE ( 'NONE', ( #3096 ), #21714, .F. ) ;
#7941=CYLINDRICAL_SURFACE ( 'NONE', #5310, 6.499999999999985789 ) ;
#7959=DIRECTION ( 'NONE',  ( -0.5089394657577702707, -0.004781488884709769391, -0.8607890319690654213 ) ) ;
#7986=DIRECTION ( 'NONE',  ( 0.5089394657577702707, 0.004781488884709769391, 0.8607890319690654213 ) ) ;
#7998=EDGE_LOOP ( 'NONE', ( #5278, #9050, #16077 ) ) ;
#8014=VECTOR ( 'NONE', #5225, 999.9999999999998863 ) ;
#8015=DIRECTION ( 'NONE',  ( 7.125109674160258889E-05, -0.9999848031710253382, 0.005512562950849898315 ) ) ;
#8024=FACE_OUTER_BOUND ( 'NONE', #13960, .T. ) ;
#8042=LINE ( 'NONE', #20336, #13733 ) ;
#8045=CIRCLE ( 'NONE', #15777, 4.400000000000003908 ) ;
#8047=DIRECTION ( 'NONE',  ( 0.01035335185279138807, 0.005513005182356417802, 0.9999312050732649393 ) ) ;
#8066=EDGE_CURVE ( 'NONE', #5759, #12590, #20265, .T. ) ;
#8078=ORIENTED_EDGE ( 'NONE', *, *, #2550, .F. ) ;
#8124=AXIS2_PLACEMENT_3D ( 'NONE', #2121, #291, #13966 ) ;
#8132=EDGE_CURVE ( 'NONE', #7137, #12590, #21881, .T. ) ;
#8146=VECTOR ( 'NONE', #10825, 999.9999999999998863 ) ;
#8175=DIRECTION ( 'NONE',  ( 7.125109674160258889E-05, -0.9999848031710253382, 0.005512562950849898315 ) ) ;
#8241=AXIS2_PLACEMENT_3D ( 'NONE', #15923, #19332, #2002 ) ;
#8286=EDGE_CURVE ( 'NONE', #17192, #14240, #10100, .T. ) ;
#8345=CARTESIAN_POINT ( 'NONE',  ( -12.58378492319879705, 109.7167104967248434, 130.3428598364639299 ) ) ;
#8357=FACE_BOUND ( 'NONE', #22078, .T. ) ;
#8399=VERTEX_POINT ( 'NONE', #20756 ) ;
#8415=AXIS2_PLACEMENT_3D ( 'NONE', #13819, #14051, #11982 ) ;
#8420=VERTEX_POINT ( 'NONE', #2269 ) ;
#8499=CARTESIAN_POINT ( 'NONE',  ( -14.37471740060550118, 109.6998846769365628, 127.3137863664913425 ) ) ;
#8539=CARTESIAN_POINT ( 'NONE',  ( -9.128127327470902941, 109.6831586031284758, 124.2118453865659546 ) ) ;
#8576=CIRCLE ( 'NONE', #12641, 4.400000000000003908 ) ;
#8596=CARTESIAN_POINT ( 'NONE',  ( -10.85595612533484911, 109.6999345499266525, 127.2773526115149281 ) ) ;
#8617=ORIENTED_EDGE ( 'NONE', *, *, #12186, .F. ) ;
#8623=LINE ( 'NONE', #7143, #17400 ) ;
#8673=EDGE_CURVE ( 'NONE', #18526, #14240, #16529, .T. ) ;
#8704=CARTESIAN_POINT ( 'NONE',  ( -12.58378492319879527, 109.7167104967248434, 130.3428598364639299 ) ) ;
#8705=CARTESIAN_POINT ( 'NONE',  ( -12.64688860274155324, 109.6831087301383860, 124.2482791415423691 ) ) ;
#8712=VERTEX_POINT ( 'NONE', #4650 ) ;
#8784=DIRECTION ( 'NONE',  ( 0.4910069343201003411, -0.004767316193522950878, -0.8711426192914036859 ) ) ;
#8884=CIRCLE ( 'NONE', #9246, 0.3999999999999986899 ) ;
#8885=ORIENTED_EDGE ( 'NONE', *, *, #20711, .F. ) ;
#8894=VECTOR ( 'NONE', #7643, 1000.000000000000114 ) ;
#8910=CARTESIAN_POINT ( 'NONE',  ( -10.85624112972181621, 113.6998737626107641, 127.2553023597115498 ) ) ;
#8924=CARTESIAN_POINT ( 'NONE',  ( -10.85340889862633595, 73.95047783656255547, 127.4744267370078177 ) ) ;
#8972=ORIENTED_EDGE ( 'NONE', *, *, #22556, .T. ) ;
#9034=EDGE_CURVE ( 'NONE', #4443, #13282, #19462, .T. ) ;
#9047=DIRECTION ( 'NONE',  ( 0.01035335185279143318, 0.005513005182356926943, 0.9999312050732649393 ) ) ;
#9050=ORIENTED_EDGE ( 'NONE', *, *, #12293, .T. ) ;
#9127=ORIENTED_EDGE ( 'NONE', *, *, #12004, .F. ) ;
#9137=CIRCLE ( 'NONE', #1455, 3.047499999999988329 ) ;
#9171=CARTESIAN_POINT ( 'NONE',  ( -10.85608148985439492, 111.4593827568422171, 127.2676533951182307 ) ) ;
#9193=EDGE_CURVE ( 'NONE', #11275, #15988, #7381, .T. ) ;
#9226=EDGE_CURVE ( 'NONE', #15988, #7332, #13635, .T. ) ;
#9236=DIRECTION ( 'NONE',  ( 7.125109674160258889E-05, -0.9999848031710252272, 0.005512562950849897447 ) ) ;
#9246=AXIS2_PLACEMENT_3D ( 'NONE', #5027, #13558, #20884 ) ;
#9290=ORIENTED_EDGE ( 'NONE', *, *, #21263, .T. ) ;
#9319=VERTEX_POINT ( 'NONE', #21436 ) ;
#9370=ADVANCED_FACE ( 'NONE', ( #12618 ), #10989, .T. ) ;
#9378=DIRECTION ( 'NONE',  ( 0.009001891267206851843, -0.4952179990463990711, 0.8687221071056580035 ) ) ;
#9390=DIRECTION ( 'NONE',  ( 0.01035335185279143318, 0.005513005182356926943, 0.9999312050732649393 ) ) ;
#9458=DIRECTION ( 'NONE',  ( 7.125109674160258889E-05, -0.9999848031710252272, 0.005512562950849897447 ) ) ;
#9526=EDGE_CURVE ( 'NONE', #13282, #18526, #6806, .T. ) ;
#9547=ADVANCED_FACE ( 'NONE', ( #5187 ), #17399, .F. ) ;
#9550=DIRECTION ( 'NONE',  ( -0.5089394657577703818, -0.004781488884709769391, -0.8607890319690654213 ) ) ;
#9552=PRODUCT_DEFINITION_FORMATION_WITH_SPECIFIED_SOURCE ( 'ANY', '', #9749, .NOT_KNOWN. ) ;
#9589=VECTOR ( 'NONE', #6098, 1000.000000000000000 ) ;
#9601=( GEOMETRIC_REPRESENTATION_CONTEXT ( 3 ) GLOBAL_UNCERTAINTY_ASSIGNED_CONTEXT ( ( #14075 ) ) GLOBAL_UNIT_ASSIGNED_CONTEXT ( ( #5329, #523, #20022 ) ) REPRESENTATION_CONTEXT ( 'NONE', 'WORKASPACE' ) );
#9612=VERTEX_POINT ( 'NONE', #10494 ) ;
#9644=EDGE_LOOP ( 'NONE', ( #11105, #13418 ) ) ;
#9655=DIRECTION ( 'NONE',  ( 7.125109674160258889E-05, -0.9999848031710252272, 0.005512562950849897447 ) ) ;
#9684=FACE_OUTER_BOUND ( 'NONE', #11134, .T. ) ;
#9694=ORIENTED_EDGE ( 'NONE', *, *, #17363, .T. ) ;
#9714=ORIENTED_EDGE ( 'NONE', *, *, #9226, .F. ) ;
#9749=PRODUCT ( 'Socket Head Cap Screw L', 'Socket Head Cap Screw L', '', ( #18498 ) ) ;
#9771=FACE_OUTER_BOUND ( 'NONE', #10268, .T. ) ;
#9789=LINE ( 'NONE', #1402, #15921 ) ;
#9797=ADVANCED_FACE ( 'NONE', ( #15207 ), #7941, .T. ) ;
#9817=DIRECTION ( 'NONE',  ( -0.9999464000778708339, -1.417269118681738834E-05, 0.01035358732233848493 ) ) ;
#9828=DIRECTION ( 'NONE',  ( -7.125109674160258889E-05, 0.9999848031710252272, -0.005512562950849897447 ) ) ;
#9843=AXIS2_PLACEMENT_3D ( 'NONE', #725, #7721, #21927 ) ;
#9870=PRODUCT_DEFINITION ( 'UNKNOWN', '', #9552, #15953 ) ;
#9909=DIRECTION ( 'NONE',  ( 0.01035335185279143318, 0.005513005182356926943, 0.9999312050732649393 ) ) ;
#9964=MANIFOLD_SOLID_BREP ( 'Stock-MAS-425-1', #17017 ) ;
#9972=VECTOR ( 'NONE', #7986, 1000.000000000000114 ) ;
#9974=CARTESIAN_POINT ( 'NONE',  ( -10.90116789308776113, 162.9865723938430051, 122.9837558165935292 ) ) ;
#9990=DIRECTION ( 'NONE',  ( 0.01035335185279153900, 0.005513005182355262476, 0.9999312050732647172 ) ) ;
#10015=VERTEX_POINT ( 'NONE', #9171 ) ;
#10098=CARTESIAN_POINT ( 'NONE',  ( -10.85567112094788200, 105.6999953372425551, 127.2994028633183348 ) ) ;
#10100=LINE ( 'NONE', #1705, #20160 ) ;
#10108=VERTEX_POINT ( 'NONE', #18370 ) ;
#10139=PLANE ( 'NONE',  #19492 ) ;
#10198=LINE ( 'NONE', #19367, #14112 ) ;
#10268=EDGE_LOOP ( 'NONE', ( #19543, #12624, #8885, #21229 ) ) ;
#10335=ADVANCED_FACE ( 'NONE', ( #2539 ), #7481, .F. ) ;
#10341=ORIENTED_EDGE ( 'NONE', *, *, #20033, .F. ) ;
#10383=AXIS2_PLACEMENT_3D ( 'NONE', #19712, #3543, #17580 ) ;
#10389=ORIENTED_EDGE ( 'NONE', *, *, #9526, .F. ) ;
#10402=DIRECTION ( 'NONE',  ( 0.5089394657577704928, 0.004781488884709768523, 0.8607890319690653103 ) ) ;
#10428=CARTESIAN_POINT ( 'NONE',  ( -10.88750796510623076, 109.6831336666334380, 124.2300622640541548 ) ) ;
#10494=CARTESIAN_POINT ( 'NONE',  ( -9.065023647928146744, 109.7167603697149474, 130.3064260814875013 ) ) ;
#10601=VERTEX_POINT ( 'NONE', #5903 ) ;
#10669=CARTESIAN_POINT ( 'NONE',  ( -10.89768303757167800, 114.0778156631497353, 123.2533725142381229 ) ) ;
#10686=AXIS2_PLACEMENT_3D ( 'NONE', #4179, #18311, #633 ) ;
#10713=VECTOR ( 'NONE', #4563, 999.9999999999998863 ) ;
#10777=DIRECTION ( 'NONE',  ( 0.01035335185279153900, 0.005513005182355262476, 0.9999312050732647172 ) ) ;
#10798=EDGE_LOOP ( 'NONE', ( #15151, #16662, #4755 ) ) ;
#10821=DIRECTION ( 'NONE',  ( 0.01035335185279134471, 0.005513005182356394383, 0.9999312050732649393 ) ) ;
#10825=DIRECTION ( 'NONE',  ( 7.125109674160258889E-05, -0.9999848031710253382, 0.005512562950849898315 ) ) ;
#10843=ORIENTED_EDGE ( 'NONE', *, *, #6740, .F. ) ;
#10851=LINE ( 'NONE', #3599, #4341 ) ;
#10869=EDGE_LOOP ( 'NONE', ( #8617, #9694, #11434, #6289 ) ) ;
#10874=CARTESIAN_POINT ( 'NONE',  ( -14.37471740060550118, 109.6998846769365628, 127.3137863664913425 ) ) ;
#10886=CYLINDRICAL_SURFACE ( 'NONE', #12098, 6.499999999999985789 ) ;
#10989=PLANE ( 'NONE',  #18742 ) ;
#11014=CARTESIAN_POINT ( 'NONE',  ( -12.58378492319879527, 109.7167104967248434, 130.3428598364639299 ) ) ;
#11063=VECTOR ( 'NONE', #9550, 1000.000000000000000 ) ;
#11090=CIRCLE ( 'NONE', #15160, 6.499999999999985789 ) ;
#11105=ORIENTED_EDGE ( 'NONE', *, *, #19314, .F. ) ;
#11134=EDGE_LOOP ( 'NONE', ( #16838, #16505, #8972, #21453 ) ) ;
#11183=ADVANCED_FACE ( 'NONE', ( #2457 ), #18307, .T. ) ;
#11221=CARTESIAN_POINT ( 'NONE',  ( -7.337194850064199692, 109.6999844229167564, 127.2409188565385421 ) ) ;
#11275=VERTEX_POINT ( 'NONE', #18752 ) ;
#11295=PLANE ( 'NONE',  #15874 ) ;
#11349=CARTESIAN_POINT ( 'NONE',  ( -9.065023647928146744, 109.7167603697149474, 130.3064260814875013 ) ) ;
#11351=CARTESIAN_POINT ( 'NONE',  ( -10.82553926660208354, 163.7173592118130045, 130.2889465353590310 ) ) ;
#11357=LINE ( 'NONE', #8345, #18517 ) ;
#11366=CIRCLE ( 'NONE', #19426, 3.047499999999988329 ) ;
#11413=PLANE ( 'NONE',  #15214 ) ;
#11434=ORIENTED_EDGE ( 'NONE', *, *, #8132, .T. ) ;
#11478=CARTESIAN_POINT ( 'NONE',  ( -7.337194850064199692, 109.6999844229167564, 127.2409188565385421 ) ) ;
#11496=CARTESIAN_POINT ( 'NONE',  ( -10.85626963016051150, 114.0998676838791681, 127.2530973345311907 ) ) ;
#11519=ORIENTED_EDGE ( 'NONE', *, *, #12293, .F. ) ;
#11560=CARTESIAN_POINT ( 'NONE',  ( -10.85626963016051150, 114.0998676838791681, 127.2530973345311907 ) ) ;
#11603=DIRECTION ( 'NONE',  ( 7.125109674160258889E-05, -0.9999848031710252272, 0.005512562950849897447 ) ) ;
#11638=FACE_BOUND ( 'NONE', #19085, .T. ) ;
#11639=LINE ( 'NONE', #22177, #16486 ) ;
#11653=EDGE_CURVE ( 'NONE', #19436, #8712, #8042, .T. ) ;
#11662=ORIENTED_EDGE ( 'NONE', *, *, #2912, .F. ) ;
#11676=VERTEX_POINT ( 'NONE', #16798 ) ;
#11723=ORIENTED_EDGE ( 'NONE', *, *, #21545, .F. ) ;
#11751=CARTESIAN_POINT ( 'NONE',  ( -12.64660359835458792, 105.6831695174542745, 124.2703293933457758 ) ) ;
#11865=ORIENTED_EDGE ( 'NONE', *, *, #20218, .T. ) ;
#11920=EDGE_LOOP ( 'NONE', ( #2904, #13088, #135, #4451 ) ) ;
#11921=VECTOR ( 'NONE', #12124, 999.9999999999998863 ) ;
#11938=DIRECTION ( 'NONE',  ( 0.01035335185279129787, 0.005513005182357351951, 0.9999312050732647172 ) ) ;
#11981=DIRECTION ( 'NONE',  ( 0.4910069343201003411, -0.004767316193522950878, -0.8711426192914036859 ) ) ;
#11982=DIRECTION ( 'NONE',  ( 0.01035335185279115042, 0.005513005182354825326, 0.9999312050732648283 ) ) ;
#12004=EDGE_CURVE ( 'NONE', #5453, #8420, #11357, .T. ) ;
#12013=ORIENTED_EDGE ( 'NONE', *, *, #4318, .T. ) ;
#12022=CARTESIAN_POINT ( 'NONE',  ( -9.064738643541179641, 105.7168211570308500, 130.3284763332909222 ) ) ;
#12023=ORIENTED_EDGE ( 'NONE', *, *, #8286, .T. ) ;
#12069=DIRECTION ( 'NONE',  ( 0.000000000000000000, 0.000000000000000000, 1.000000000000000000 ) ) ;
#12085=PLANE ( 'NONE',  #2981 ) ;
#12098=AXIS2_PLACEMENT_3D ( 'NONE', #8924, #15971, #3532 ) ;
#12099=ORIENTED_EDGE ( 'NONE', *, *, #6740, .T. ) ;
#12100=FACE_OUTER_BOUND ( 'NONE', #4513, .T. ) ;
#12124=DIRECTION ( 'NONE',  ( 7.125109674160258889E-05, -0.9999848031710253382, 0.005512562950849898315 ) ) ;
#12140=EDGE_LOOP ( 'NONE', ( #15748, #13677, #458, #9290 ) ) ;
#12160=DIRECTION ( 'NONE',  ( 0.9999464000778708339, 1.417269118681874529E-05, -0.01035358732233823860 ) ) ;
#12173=VECTOR ( 'NONE', #2878, 1000.000000000000114 ) ;
#12186=EDGE_CURVE ( 'NONE', #9319, #5759, #10198, .T. ) ;
#12202=ORIENTED_EDGE ( 'NONE', *, *, #4318, .F. ) ;
#12281=CIRCLE ( 'NONE', #8241, 4.000000000000006217 ) ;
#12293=EDGE_CURVE ( 'NONE', #7332, #555, #16311, .T. ) ;
#12298=CARTESIAN_POINT ( 'NONE',  ( -10.92353791676496222, 113.6640392289254322, 120.7557495267353147 ) ) ;
#12360=PRODUCT_DEFINITION_SHAPE ( 'NONE', 'NONE',  #9870 ) ;
#12408=ORIENTED_EDGE ( 'NONE', *, *, #9193, .T. ) ;
#12436=ORIENTED_EDGE ( 'NONE', *, *, #5551, .F. ) ;
#12541=ORIENTED_EDGE ( 'NONE', *, *, #2912, .T. ) ;
#12566=CYLINDRICAL_SURFACE ( 'NONE', #19123, 4.000000000000006217 ) ;
#12590=VERTEX_POINT ( 'NONE', #720 ) ;
#12618=FACE_OUTER_BOUND ( 'NONE', #5673, .T. ) ;
#12624=ORIENTED_EDGE ( 'NONE', *, *, #7843, .T. ) ;
#12638=CARTESIAN_POINT ( 'NONE',  ( -9.064738643541179641, 105.7168211570308500, 130.3284763332909222 ) ) ;
#12641=AXIS2_PLACEMENT_3D ( 'NONE', #8910, #15960, #5456 ) ;
#12642=ORIENTED_EDGE ( 'NONE', *, *, #22626, .F. ) ;
#12652=DIRECTION ( 'NONE',  ( -0.01035335185279007662, -0.005513005182356926943, -0.9999312050732648283 ) ) ;
#12674=ORIENTED_EDGE ( 'NONE', *, *, #15406, .T. ) ;
#12688=DIRECTION ( 'NONE',  ( 0.01035335185279151644, 0.005513005182356664133, 0.9999312050732649393 ) ) ;
#12727=CARTESIAN_POINT ( 'NONE',  ( -9.065023647928146744, 109.7167603697149474, 130.3064260814875013 ) ) ;
#12738=CARTESIAN_POINT ( 'NONE',  ( -10.78894434267867197, 113.7357082962960817, 133.7548551926877280 ) ) ;
#12740=EDGE_CURVE ( 'NONE', #12590, #5091, #9789, .T. ) ;
#12760=ORIENTED_EDGE ( 'NONE', *, *, #2424, .T. ) ;
#12778=CARTESIAN_POINT ( 'NONE',  ( -10.85567112094788200, 105.6999953372425551, 127.2994028633183348 ) ) ;
#12817=CARTESIAN_POINT ( 'NONE',  ( -9.127842323083935838, 105.6832193904443784, 124.2338956383693613 ) ) ;
#12834=VECTOR ( 'NONE', #12160, 1000.000000000000227 ) ;
#12859=DIRECTION ( 'NONE',  ( 0.01035335185279143318, 0.005513005182356926943, 0.9999312050732649393 ) ) ;
#12873=ORIENTED_EDGE ( 'NONE', *, *, #4449, .F. ) ;
#12890=LINE ( 'NONE', #19152, #5459 ) ;
#12936=ORIENTED_EDGE ( 'NONE', *, *, #11653, .F. ) ;
#13086=DIRECTION ( 'NONE',  ( 7.125109674160258889E-05, -0.9999848031710253382, 0.005512562950849898315 ) ) ;
#13088=ORIENTED_EDGE ( 'NONE', *, *, #7659, .T. ) ;
#13136=ORIENTED_EDGE ( 'NONE', *, *, #19314, .T. ) ;
#13148=FACE_OUTER_BOUND ( 'NONE', #19757, .T. ) ;
#13234=CARTESIAN_POINT ( 'NONE',  ( -12.64688860274155324, 109.6831087301383860, 124.2482791415423691 ) ) ;
#13282=VERTEX_POINT ( 'NONE', #6390 ) ;
#13303=CARTESIAN_POINT ( 'NONE',  ( -7.337194850064199692, 109.6999844229167564, 127.2409188565385421 ) ) ;
#13371=VECTOR ( 'NONE', #4837, 1000.000000000000227 ) ;
#13418=ORIENTED_EDGE ( 'NONE', *, *, #17363, .F. ) ;
#13516=CARTESIAN_POINT ( 'NONE',  ( -7.337194850064199692, 109.6999844229167564, 127.2409188565385421 ) ) ;
#13544=DIRECTION ( 'NONE',  ( 0.9999464000778708339, 1.417269118681874529E-05, -0.01035358732233823860 ) ) ;
#13558=DIRECTION ( 'NONE',  ( -0.9999464000778710560, -1.417269118681194361E-05, 0.01035358732233947372 ) ) ;
#13635=CIRCLE ( 'NONE', #2233, 3.047499999999988329 ) ;
#13677=ORIENTED_EDGE ( 'NONE', *, *, #8066, .T. ) ;
#13682=DIRECTION ( 'NONE',  ( 7.125109674160258889E-05, -0.9999848031710252272, 0.005512562950849897447 ) ) ;
#13733=VECTOR ( 'NONE', #6550, 999.9999999999998863 ) ;
#13768=DIRECTION ( 'NONE',  ( -0.008930640170465353744, -0.5047668041246317072, -0.8632095441548079950 ) ) ;
#13819=CARTESIAN_POINT ( 'NONE',  ( -10.85980368455889433, 163.6991139211620236, 126.9796742121690443 ) ) ;
#13831=CARTESIAN_POINT ( 'NONE',  ( -7.337194850064199692, 109.6999844229167564, 127.2409188565385421 ) ) ;
#13873=DIRECTION ( 'NONE',  ( -0.007270543169446415203, -0.7109943187548720678, -0.7031601651830943212 ) ) ;
#13960=EDGE_LOOP ( 'NONE', ( #13136, #5194, #11723, #20698 ) ) ;
#13966=DIRECTION ( 'NONE',  ( 0.01035335185279115042, 0.005513005182354825326, 0.9999312050732648283 ) ) ;
#13969=ORIENTED_EDGE ( 'NONE', *, *, #22556, .F. ) ;
#13999=FACE_OUTER_BOUND ( 'NONE', #22612, .T. ) ;
#14051=DIRECTION ( 'NONE',  ( 7.125109674160258889E-05, -0.9999848031710252272, 0.005512562950849897447 ) ) ;
#14075=UNCERTAINTY_MEASURE_WITH_UNIT (LENGTH_MEASURE( 1.000000000000000082E-05 ), #5329, 'distance_accuracy_value', 'NONE');
#14112=VECTOR ( 'NONE', #13873, 1000.000000000000000 ) ;
#14128=VECTOR ( 'NONE', #17275, 1000.000000000000000 ) ;
#14187=ORIENTED_EDGE ( 'NONE', *, *, #17013, .F. ) ;
#14193=EDGE_LOOP ( 'NONE', ( #20332, #2467, #5998, #7029, #3801 ) ) ;
#14216=ORIENTED_EDGE ( 'NONE', *, *, #612, .T. ) ;
#14218=DIRECTION ( 'NONE',  ( 7.125109674160258889E-05, -0.9999848031710252272, 0.005512562950849897447 ) ) ;
#14240=VERTEX_POINT ( 'NONE', #12817 ) ;
#14345=LINE ( 'NONE', #3630, #2580 ) ;
#14381=AXIS2_PLACEMENT_3D ( 'NONE', #15672, #1537, #17157 ) ;
#14456=CARTESIAN_POINT ( 'NONE',  ( -10.85595612533484911, 109.6999345499266525, 127.2773526115149281 ) ) ;
#14457=AXIS2_PLACEMENT_3D ( 'NONE', #11560, #9828, #16846 ) ;
#14472=AXIS2_PLACEMENT_3D ( 'NONE', #20117, #16616, #7959 ) ;
#14507=DIRECTION ( 'NONE',  ( 7.125109674160258889E-05, -0.9999848031710252272, 0.005512562950849897447 ) ) ;
#14584=EDGE_CURVE ( 'NONE', #22007, #5091, #12281, .T. ) ;
#14663=CYLINDRICAL_SURFACE ( 'NONE', #15069, 4.000000000000006217 ) ;
#14688=LINE ( 'NONE', #5800, #9972 ) ;
#14712=EDGE_CURVE ( 'NONE', #7332, #4443, #19245, .T. ) ;
#14731=ADVANCED_FACE ( 'NONE', ( #8357, #1030 ), #5019, .T. ) ;
#14818=ADVANCED_FACE ( 'NONE', ( #8024 ), #15515, .T. ) ;
#14842=CIRCLE ( 'NONE', #17779, 6.499999999999985789 ) ;
#15057=CARTESIAN_POINT ( 'NONE',  ( -10.85572812182527613, 106.4999831797793775, 127.2949928129576733 ) ) ;
#15069=AXIS2_PLACEMENT_3D ( 'NONE', #20020, #9458, #2354 ) ;
#15083=VERTEX_POINT ( 'NONE', #12738 ) ;
#15106=ORIENTED_EDGE ( 'NONE', *, *, #9193, .F. ) ;
#15129=ADVANCED_FACE ( 'NONE', ( #4098 ), #16536, .T. ) ;
#15151=ORIENTED_EDGE ( 'NONE', *, *, #5094, .F. ) ;
#15160=AXIS2_PLACEMENT_3D ( 'NONE', #6539, #20767, #19160 ) ;
#15197=EDGE_LOOP ( 'NONE', ( #12642, #441, #3009, #1159, #16452 ) ) ;
#15207=FACE_OUTER_BOUND ( 'NONE', #3946, .T. ) ;
#15214=AXIS2_PLACEMENT_3D ( 'NONE', #18425, #2693, #15556 ) ;
#15221=DIRECTION ( 'NONE',  ( 0.01035335185279143318, 0.005513005182356926943, 0.9999312050732649393 ) ) ;
#15235=CARTESIAN_POINT ( 'NONE',  ( -10.85626963016051150, 114.0998676838791681, 127.2530973345311907 ) ) ;
#15348=AXIS2_PLACEMENT_3D ( 'NONE', #8704, #1833, #9047 ) ;
#15402=DIRECTION ( 'NONE',  ( -0.01035335185279143318, -0.005513005182356926943, -0.9999312050732649393 ) ) ;
#15405=AXIS2_PLACEMENT_3D ( 'NONE', #2178, #14507, #10821 ) ;
#15406=EDGE_CURVE ( 'NONE', #22002, #8420, #7188, .T. ) ;
#15413=ORIENTED_EDGE ( 'NONE', *, *, #14584, .F. ) ;
#15415=CARTESIAN_POINT ( 'NONE',  ( -10.85624112972181621, 113.6998737626107641, 127.2553023597115498 ) ) ;
#15421=CARTESIAN_POINT ( 'NONE',  ( -9.064738643541179641, 105.7168211570308500, 130.3284763332909222 ) ) ;
#15515=CONICAL_SURFACE ( 'NONE', #1923, 3.309500000000006992, 0.7853981633974710386 ) ;
#15531=LINE ( 'NONE', #15421, #12173 ) ;
#15550=DIRECTION ( 'NONE',  ( 7.125109674160258889E-05, -0.9999848031710252272, 0.005512562950849896580 ) ) ;
#15556=DIRECTION ( 'NONE',  ( 0.01035335185279143318, 0.005513005182356926943, 0.9999312050732649393 ) ) ;
#15573=ORIENTED_EDGE ( 'NONE', *, *, #8673, .F. ) ;
#15600=DIRECTION ( 'NONE',  ( -0.9999464000778708339, -1.417269118681738834E-05, 0.01035358732233848493 ) ) ;
#15653=ORIENTED_EDGE ( 'NONE', *, *, #9034, .F. ) ;
#15666=DIRECTION ( 'NONE',  ( 7.125109674160258889E-05, -0.9999848031710253382, 0.005512562950849898315 ) ) ;
#15672=CARTESIAN_POINT ( 'NONE',  ( -10.90182437831279572, 114.0756104610767920, 122.8534000322088247 ) ) ;
#15748=ORIENTED_EDGE ( 'NONE', *, *, #7659, .F. ) ;
#15756=PLANE ( 'NONE',  #15348 ) ;
#15777=AXIS2_PLACEMENT_3D ( 'NONE', #19806, #16640, #543 ) ;
#15874=AXIS2_PLACEMENT_3D ( 'NONE', #18299, #18634, #9909 ) ;
#15887=EDGE_LOOP ( 'NONE', ( #5352, #581 ) ) ;
#15896=CARTESIAN_POINT ( 'NONE',  ( -10.89482230603750246, 73.92842581583312267, 123.4747019167147499 ) ) ;
#15921=VECTOR ( 'NONE', #8175, 999.9999999999998863 ) ;
#15923=CARTESIAN_POINT ( 'NONE',  ( -10.85626963016051150, 114.0998676838791681, 127.2530973345311907 ) ) ;
#15953=PRODUCT_DEFINITION_CONTEXT ( 'detailed design', #1483, 'design' ) ;
#15960=DIRECTION ( 'NONE',  ( 7.125109674160258889E-05, -0.9999848031710252272, 0.005512562950849897447 ) ) ;
#15971=DIRECTION ( 'NONE',  ( 7.125109674160258889E-05, -0.9999848031710252272, 0.005512562950849897447 ) ) ;
#15988=VERTEX_POINT ( 'NONE', #20500 ) ;
#16028=CARTESIAN_POINT ( 'NONE',  ( -14.37471740060550118, 109.6998846769365628, 127.3137863664913425 ) ) ;
#16035=APPLICATION_CONTEXT ( 'automotive_design' ) ;
#16058=ADVANCED_FACE ( 'NONE', ( #7065 ), #6291, .T. ) ;
#16077=ORIENTED_EDGE ( 'NONE', *, *, #3017, .T. ) ;
#16096=ADVANCED_FACE ( 'NONE', ( #16167 ), #410, .T. ) ;
#16103=PLANE ( 'NONE',  #3732 ) ;
#16126=EDGE_LOOP ( 'NONE', ( #14187, #16394, #12408, #19935, #4966 ) ) ;
#16162=EDGE_CURVE ( 'NONE', #9612, #11275, #20126, .T. ) ;
#16167=FACE_OUTER_BOUND ( 'NONE', #9644, .T. ) ;
#16256=EDGE_LOOP ( 'NONE', ( #14216, #19005, #6008, #1790 ) ) ;
#16288=DIRECTION ( 'NONE',  ( 0.01035335185279153900, 0.005513005182355262476, 0.9999312050732647172 ) ) ;
#16311=LINE ( 'NONE', #2140, #8894 ) ;
#16347=AXIS2_PLACEMENT_3D ( 'NONE', #17117, #11603, #9990 ) ;
#16394=ORIENTED_EDGE ( 'NONE', *, *, #17151, .T. ) ;
#16450=ADVANCED_FACE ( 'NONE', ( #17753 ), #12566, .T. ) ;
#16452=ORIENTED_EDGE ( 'NONE', *, *, #8673, .T. ) ;
#16486=VECTOR ( 'NONE', #11981, 1000.000000000000114 ) ;
#16505=ORIENTED_EDGE ( 'NONE', *, *, #1244, .F. ) ;
#16529=LINE ( 'NONE', #1006, #1135 ) ;
#16536=PLANE ( 'NONE',  #19134 ) ;
#16616=DIRECTION ( 'NONE',  ( 0.8608023089638390246, -0.002744228680570686644, -0.5089320721780777879 ) ) ;
#16640=DIRECTION ( 'NONE',  ( 7.125109674160258889E-05, -0.9999848031710252272, 0.005512562950849897447 ) ) ;
#16662=ORIENTED_EDGE ( 'NONE', *, *, #20733, .F. ) ;
#16680=UNCERTAINTY_MEASURE_WITH_UNIT (LENGTH_MEASURE( 1.000000000000000082E-05 ), #5156, 'distance_accuracy_value', 'NONE');
#16752=LINE ( 'NONE', #1000, #69 ) ;
#16797=LINE ( 'NONE', #20094, #11063 ) ;
#16798=CARTESIAN_POINT ( 'NONE',  ( -10.81068638156953376, 113.7241309854131259, 131.6549996620339300 ) ) ;
#16810=ORIENTED_EDGE ( 'NONE', *, *, #18788, .T. ) ;
#16823=ADVANCED_FACE ( 'NONE', ( #12100 ), #21556, .T. ) ;
#16838=ORIENTED_EDGE ( 'NONE', *, *, #5883, .F. ) ;
#16846=DIRECTION ( 'NONE',  ( -0.01035335185279159971, -0.005513005182356926943, -0.9999312050732648283 ) ) ;
#16929=FACE_OUTER_BOUND ( 'NONE', #14193, .T. ) ;
#16971=EDGE_CURVE ( 'NONE', #19627, #8399, #4225, .T. ) ;
#17001=VECTOR ( 'NONE', #6299, 999.9999999999998863 ) ;
#17013=EDGE_CURVE ( 'NONE', #10015, #4443, #17446, .T. ) ;
#17017=CLOSED_SHELL ( 'NONE', ( #1907, #4576, #3043, #3025, #16450, #14818, #7304, #16096, #16058, #6281, #14731, #9797, #3648, #19579, #11183, #10335, #21440, #20869, #18096, #9547, #9370, #15129, #20001, #21463, #1568, #16823, #7893 ) ) ;
#17100=EDGE_CURVE ( 'NONE', #10108, #19627, #549, .T. ) ;
#17117=CARTESIAN_POINT ( 'NONE',  ( -10.85595612533484911, 109.6999345499266525, 127.2773526115149281 ) ) ;
#17136=EDGE_CURVE ( 'NONE', #8712, #8420, #14688, .T. ) ;
#17151=EDGE_CURVE ( 'NONE', #10015, #11275, #16752, .T. ) ;
#17157=DIRECTION ( 'NONE',  ( -0.01035358732338034077, 0.000000000000000000, -0.9999464001782980560 ) ) ;
#17192=VERTEX_POINT ( 'NONE', #11751 ) ;
#17275=DIRECTION ( 'NONE',  ( -0.5089394657577703818, -0.004781488884709769391, -0.8607890319690654213 ) ) ;
#17357=CARTESIAN_POINT ( 'NONE',  ( -12.58378492319879705, 109.7167104967248434, 130.3428598364639299 ) ) ;
#17363=EDGE_CURVE ( 'NONE', #9319, #7137, #20149, .T. ) ;
#17388=ORIENTED_EDGE ( 'NONE', *, *, #5044, .T. ) ;
#17399=PLANE ( 'NONE',  #19608 ) ;
#17400=VECTOR ( 'NONE', #15666, 999.9999999999998863 ) ;
#17446=LINE ( 'NONE', #10428, #20976 ) ;
#17535=CARTESIAN_POINT ( 'NONE',  ( -10.85595612533484911, 109.6999345499266525, 127.2773526115149281 ) ) ;
#17559=CONICAL_SURFACE ( 'NONE', #9843, 5.700000000000003730, 0.7853981633974482790 ) ;
#17580=DIRECTION ( 'NONE',  ( 0.01035335185279151644, 0.005513005182360133580, 0.9999312050732649393 ) ) ;
#17635=DIRECTION ( 'NONE',  ( 0.5089394657577702707, 0.004781488884709769391, 0.8607890319690654213 ) ) ;
#17688=DIRECTION ( 'NONE',  ( 7.125109674160258889E-05, -0.9999848031710252272, 0.005512562950849897447 ) ) ;
#17753=FACE_OUTER_BOUND ( 'NONE', #11920, .T. ) ;
#17779=AXIS2_PLACEMENT_3D ( 'NONE', #15415, #20207, #18714 ) ;
#17799=DIRECTION ( 'NONE',  ( 0.4910069343201003411, -0.004767316193522950878, -0.8711426192914037969 ) ) ;
#17838=VERTEX_POINT ( 'NONE', #22186 ) ;
#18010=LINE ( 'NONE', #10874, #21956 ) ;
#18027=VECTOR ( 'NONE', #15600, 1000.000000000000227 ) ;
#18050=EDGE_CURVE ( 'NONE', #22002, #8399, #15531, .T. ) ;
#18093=VECTOR ( 'NONE', #792, 999.9999999999998863 ) ;
#18096=ADVANCED_FACE ( 'NONE', ( #122 ), #16103, .F. ) ;
#18131=DIRECTION ( 'NONE',  ( 0.01035335185279153900, 0.005513005182355262476, 0.9999312050732647172 ) ) ;
#18149=CARTESIAN_POINT ( 'NONE',  ( -12.58378492319879527, 109.7167104967248434, 130.3428598364639299 ) ) ;
#18280=DIRECTION ( 'NONE',  ( 0.9999464000778708339, 1.417269118681738664E-05, -0.01035358732233848666 ) ) ;
#18299=CARTESIAN_POINT ( 'NONE',  ( -10.85567112094788200, 105.6999953372425551, 127.2994028633183348 ) ) ;
#18307=PLANE ( 'NONE',  #14472 ) ;
#18311=DIRECTION ( 'NONE',  ( 7.125109674160258889E-05, -0.9999848031710252272, 0.005512562950849897447 ) ) ;
#18370=CARTESIAN_POINT ( 'NONE',  ( -8.201109248996173662, 109.7083723963158519, 128.7736724690130359 ) ) ;
#18399=LINE ( 'NONE', #5987, #9589 ) ;
#18425=CARTESIAN_POINT ( 'NONE',  ( -12.58378492319879527, 109.7167104967248434, 130.3428598364639299 ) ) ;
#18496=DIRECTION ( 'NONE',  ( -7.125109674160258889E-05, 0.9999848031710252272, -0.005512562950849896580 ) ) ;
#18498=PRODUCT_CONTEXT ( 'NONE', #16035, 'mechanical' ) ;
#18517=VECTOR ( 'NONE', #8015, 999.9999999999998863 ) ;
#18526=VERTEX_POINT ( 'NONE', #8539 ) ;
#18598=CARTESIAN_POINT ( 'NONE',  ( -10.85980368455889433, 163.6991139211620236, 126.9796742121690443 ) ) ;
#18634=DIRECTION ( 'NONE',  ( 7.125109674160258889E-05, -0.9999848031710252272, 0.005512562950849896580 ) ) ;
#18671=ORIENTED_EDGE ( 'NONE', *, *, #20711, .T. ) ;
#18714=DIRECTION ( 'NONE',  ( 0.01035335185279138807, 0.005513005182356417802, 0.9999312050732649393 ) ) ;
#18742=AXIS2_PLACEMENT_3D ( 'NONE', #3528, #5698, #7309 ) ;
#18752=CARTESIAN_POINT ( 'NONE',  ( -10.82440428556347101, 109.7167354332198812, 130.3246429589757156 ) ) ;
#18786=FACE_OUTER_BOUND ( 'NONE', #15197, .T. ) ;
#18788=EDGE_CURVE ( 'NONE', #18866, #15083, #11090, .T. ) ;
#18819=TOROIDAL_SURFACE ( 'NONE', #14457, 4.400000000000000355, 0.4000000000000000222 ) ;
#18866=VERTEX_POINT ( 'NONE', #12298 ) ;
#18901=ORIENTED_EDGE ( 'NONE', *, *, #4449, .T. ) ;
#18905=AXIS2_PLACEMENT_3D ( 'NONE', #19640, #2086, #18280 ) ;
#18929=DIRECTION ( 'NONE',  ( 7.125109674160258889E-05, -0.9999848031710252272, 0.005512562950849897447 ) ) ;
#18958=EDGE_LOOP ( 'NONE', ( #2447, #12099 ) ) ;
#19005=ORIENTED_EDGE ( 'NONE', *, *, #2199, .T. ) ;
#19024=AXIS2_PLACEMENT_3D ( 'NONE', #15057, #9655, #6532 ) ;
#19085=EDGE_LOOP ( 'NONE', ( #20109, #22214, #4241, #970, #2237, #12202 ) ) ;
#19113=AXIS2_PLACEMENT_3D ( 'NONE', #15235, #6481, #5065 ) ;
#19117=CIRCLE ( 'NONE', #7021, 5.699999999999990408 ) ;
#19123=AXIS2_PLACEMENT_3D ( 'NONE', #5415, #381, #12688 ) ;
#19134=AXIS2_PLACEMENT_3D ( 'NONE', #18149, #2399, #9390 ) ;
#19152=CARTESIAN_POINT ( 'NONE',  ( -12.64688860274155324, 109.6831087301383860, 124.2482791415423691 ) ) ;
#19157=EDGE_CURVE ( 'NONE', #9612, #22002, #21658, .T. ) ;
#19160=DIRECTION ( 'NONE',  ( 0.01035335185279138807, 0.005513005182356417802, 0.9999312050732649393 ) ) ;
#19175=AXIS2_PLACEMENT_3D ( 'NONE', #22447, #20851, #6737 ) ;
#19245=CIRCLE ( 'NONE', #16347, 3.047499999999988329 ) ;
#19293=FILL_AREA_STYLE ('',( #3208 ) ) ;
#19307=DIRECTION ( 'NONE',  ( 0.01035335185279151644, 0.005513005182360133580, 0.9999312050732649393 ) ) ;
#19314=EDGE_CURVE ( 'NONE', #7137, #9319, #1218, .T. ) ;
#19325=ORIENTED_EDGE ( 'NONE', *, *, #3026, .F. ) ;
#19332=DIRECTION ( 'NONE',  ( -7.125109674160258889E-05, 0.9999848031710252272, -0.005512562950849897447 ) ) ;
#19357=CARTESIAN_POINT ( 'NONE',  ( -10.91468522650879258, 105.6685712077031241, 121.5997949944007246 ) ) ;
#19367=CARTESIAN_POINT ( 'NONE',  ( -10.89406810251570867, 163.6808686305110143, 123.6704018889790717 ) ) ;
#19426=AXIS2_PLACEMENT_3D ( 'NONE', #2147, #17688, #10777 ) ;
#19436=VERTEX_POINT ( 'NONE', #7192 ) ;
#19462=CIRCLE ( 'NONE', #22375, 3.047499999999988329 ) ;
#19470=DIRECTION ( 'NONE',  ( 0.01035335185279153900, 0.005513005182355262476, 0.9999312050732647172 ) ) ;
#19492=AXIS2_PLACEMENT_3D ( 'NONE', #4945, #6790, #5054 ) ;
#19543=ORIENTED_EDGE ( 'NONE', *, *, #21263, .F. ) ;
#19575=CARTESIAN_POINT ( 'NONE',  ( -14.16912629561661063, 163.6990670166405266, 127.0139394094123304 ) ) ;
#19579=ADVANCED_FACE ( 'NONE', ( #20270 ), #18819, .F. ) ;
#19602=DIRECTION ( 'NONE',  ( -7.125109674160258889E-05, 0.9999848031710252272, -0.005512562950849897447 ) ) ;
#19608=AXIS2_PLACEMENT_3D ( 'NONE', #16028, #6701, #20709 ) ;
#19627=VERTEX_POINT ( 'NONE', #11221 ) ;
#19640=CARTESIAN_POINT ( 'NONE',  ( -9.065023647928146744, 109.7167603697149474, 130.3064260814875013 ) ) ;
#19712=CARTESIAN_POINT ( 'NONE',  ( -10.85975448567659463, 163.0086244145724379, 126.9834806368866111 ) ) ;
#19753=DIRECTION ( 'NONE',  ( 7.125109674160258889E-05, -0.9999848031710252272, 0.005512562950849897447 ) ) ;
#19757=EDGE_LOOP ( 'NONE', ( #15653, #12541, #10389 ) ) ;
#19806=CARTESIAN_POINT ( 'NONE',  ( -10.85624112972181621, 113.6998737626107641, 127.2553023597115498 ) ) ;
#19855=ORIENTED_EDGE ( 'NONE', *, *, #20990, .F. ) ;
#19935=ORIENTED_EDGE ( 'NONE', *, *, #9226, .T. ) ;
#20001=ADVANCED_FACE ( 'NONE', ( #13148 ), #11413, .T. ) ;
#20020=CARTESIAN_POINT ( 'NONE',  ( -10.85340889862633595, 73.95047783656255547, 127.4744267370078177 ) ) ;
#20022=( NAMED_UNIT ( * ) SI_UNIT ( $, .STERADIAN. ) SOLID_ANGLE_UNIT ( ) );
#20030=ORIENTED_EDGE ( 'NONE', *, *, #21205, .T. ) ;
#20033=EDGE_CURVE ( 'NONE', #11275, #5453, #2799, .T. ) ;
#20050=ORIENTED_EDGE ( 'NONE', *, *, #7843, .F. ) ;
#20060=AXIS2_PLACEMENT_3D ( 'NONE', #12778, #19753, #7596 ) ;
#20094=CARTESIAN_POINT ( 'NONE',  ( -7.336909845677233477, 105.7000452102326591, 127.2629691083419203 ) ) ;
#20109=ORIENTED_EDGE ( 'NONE', *, *, #17136, .T. ) ;
#20117=CARTESIAN_POINT ( 'NONE',  ( -14.37471740060550118, 109.6998846769365628, 127.3137863664913425 ) ) ;
#20126=LINE ( 'NONE', #7866, #21302 ) ;
#20149=CIRCLE ( 'NONE', #8415, 3.309500000000006992 ) ;
#20160=VECTOR ( 'NONE', #13544, 1000.000000000000227 ) ;
#20162=ORIENTED_EDGE ( 'NONE', *, *, #5094, .T. ) ;
#20205=AXIS2_PLACEMENT_3D ( 'NONE', #20456, #3465, #19307 ) ;
#20207=DIRECTION ( 'NONE',  ( 7.125109674160258889E-05, -0.9999848031710252272, 0.005512562950849897447 ) ) ;
#20218=EDGE_CURVE ( 'NONE', #15083, #307, #8623, .T. ) ;
#20264=ORIENTED_EDGE ( 'NONE', *, *, #16162, .T. ) ;
#20265=CIRCLE ( 'NONE', #10383, 4.000000000000006217 ) ;
#20270=FACE_OUTER_BOUND ( 'NONE', #21052, .T. ) ;
#20319=SHAPE_DEFINITION_REPRESENTATION ( #12360, #938 ) ;
#20332=ORIENTED_EDGE ( 'NONE', *, *, #18050, .F. ) ;
#20336=CARTESIAN_POINT ( 'NONE',  ( -14.37471740060550118, 109.6998846769365628, 127.3137863664913425 ) ) ;
#20456=CARTESIAN_POINT ( 'NONE',  ( -10.85975448567659463, 163.0086244145724379, 126.9834806368866111 ) ) ;
#20495=ORIENTED_EDGE ( 'NONE', *, *, #19157, .T. ) ;
#20500=CARTESIAN_POINT ( 'NONE',  ( -13.47925116190214823, 109.7082975868306960, 128.8283231014776220 ) ) ;
#20520=ORIENTED_EDGE ( 'NONE', *, *, #9034, .T. ) ;
#20635=LINE ( 'NONE', #22658, #8014 ) ;
#20646=DIRECTION ( 'NONE',  ( 7.125109674160258889E-05, -0.9999848031710252272, 0.005512562950849897447 ) ) ;
#20698=ORIENTED_EDGE ( 'NONE', *, *, #8132, .F. ) ;
#20699=ORIENTED_EDGE ( 'NONE', *, *, #2424, .F. ) ;
#20709=DIRECTION ( 'NONE',  ( -0.4910069343201003411, 0.004767316193522950878, 0.8711426192914036859 ) ) ;
#20711=EDGE_CURVE ( 'NONE', #10601, #11676, #8576, .T. ) ;
#20733=EDGE_CURVE ( 'NONE', #19627, #13282, #21863, .T. ) ;
#20756=CARTESIAN_POINT ( 'NONE',  ( -7.336909845677233477, 105.7000452102326591, 127.2629691083419203 ) ) ;
#20767=DIRECTION ( 'NONE',  ( 7.125109674160258889E-05, -0.9999848031710252272, 0.005512562950849897447 ) ) ;
#20831=LINE ( 'NONE', #5089, #11921 ) ;
#20851=DIRECTION ( 'NONE',  ( 7.125109674160258889E-05, -0.9999848031710252272, 0.005512562950849897447 ) ) ;
#20869=ADVANCED_FACE ( 'NONE', ( #18786 ), #1345, .T. ) ;
#20884=DIRECTION ( 'NONE',  ( 0.01035358732338034077, 0.000000000000000000, 0.9999464001782980560 ) ) ;
#20899=SURFACE_SIDE_STYLE ('',( #3557 ) ) ;
#20941=ORIENTED_EDGE ( 'NONE', *, *, #16162, .F. ) ;
#20976=VECTOR ( 'NONE', #13768, 1000.000000000000000 ) ;
#20986=CARTESIAN_POINT ( 'NONE',  ( -10.85567112094788200, 105.6999953372425551, 127.2994028633183348 ) ) ;
#20990=EDGE_CURVE ( 'NONE', #555, #17192, #20831, .T. ) ;
#21052=EDGE_LOOP ( 'NONE', ( #20050, #15413, #20030, #3731 ) ) ;
#21064=CARTESIAN_POINT ( 'NONE',  ( -10.88750796510622720, 109.6831336666334380, 124.2300622640541690 ) ) ;
#21100=FACE_OUTER_BOUND ( 'NONE', #16256, .T. ) ;
#21133=PRESENTATION_STYLE_ASSIGNMENT (( #22593 ) ) ;
#21205=EDGE_CURVE ( 'NONE', #22007, #10601, #418, .T. ) ;
#21229=ORIENTED_EDGE ( 'NONE', *, *, #21205, .F. ) ;
#21233=DIRECTION ( 'NONE',  ( -0.9999464000778708339, -1.417269118681874529E-05, 0.01035358732233823860 ) ) ;
#21263=EDGE_CURVE ( 'NONE', #5091, #22007, #1167, .T. ) ;
#21293=AXIS2_PLACEMENT_3D ( 'NONE', #11496, #593, #2762 ) ;
#21302=VECTOR ( 'NONE', #9817, 1000.000000000000227 ) ;
#21436=CARTESIAN_POINT ( 'NONE',  ( -10.89406810251570867, 163.6808686305110143, 123.6704018889790717 ) ) ;
#21440=ADVANCED_FACE ( 'NONE', ( #16929 ), #10139, .T. ) ;
#21453=ORIENTED_EDGE ( 'NONE', *, *, #2550, .T. ) ;
#21463=ADVANCED_FACE ( 'NONE', ( #22604 ), #12085, .T. ) ;
#21545=EDGE_CURVE ( 'NONE', #12590, #5759, #4436, .T. ) ;
#21556=PLANE ( 'NONE',  #3736 ) ;
#21605=CONICAL_SURFACE ( 'NONE', #7322, 5.700000000000003730, 0.7853981633974482790 ) ;
#21658=LINE ( 'NONE', #11349, #18093 ) ;
#21714=CONICAL_SURFACE ( 'NONE', #3764, 3.047499999999988329, 1.047197551196594523 ) ;
#21863=LINE ( 'NONE', #13303, #5650 ) ;
#21881=LINE ( 'NONE', #11351, #17001 ) ;
#21887=ORIENTED_EDGE ( 'NONE', *, *, #20990, .T. ) ;
#21927=DIRECTION ( 'NONE',  ( -0.01035335185279127358, -0.005513005182357338940, -0.9999312050732649393 ) ) ;
#21944=CIRCLE ( 'NONE', #19024, 6.500000000000013323 ) ;
#21949=EDGE_LOOP ( 'NONE', ( #2542, #12936, #18901, #12760, #5862 ) ) ;
#21956=VECTOR ( 'NONE', #8784, 1000.000000000000114 ) ;
#21977=VECTOR ( 'NONE', #4106, 1000.000000000000114 ) ;
#22002=VERTEX_POINT ( 'NONE', #12638 ) ;
#22007=VERTEX_POINT ( 'NONE', #10669 ) ;
#22078=EDGE_LOOP ( 'NONE', ( #18671, #17388 ) ) ;
#22145=ORIENTED_EDGE ( 'NONE', *, *, #3026, .T. ) ;
#22176=FACE_OUTER_BOUND ( 'NONE', #18958, .T. ) ;
#22177=CARTESIAN_POINT ( 'NONE',  ( -14.37443239621853408, 105.6999454642524654, 127.3358366182947634 ) ) ;
#22186=CARTESIAN_POINT ( 'NONE',  ( -10.92302490886842214, 106.4641486460940456, 120.7954399799814382 ) ) ;
#22214=ORIENTED_EDGE ( 'NONE', *, *, #15406, .F. ) ;
#22251=DIRECTION ( 'NONE',  ( 0.01035335185279153900, 0.005513005182355262476, 0.9999312050732647172 ) ) ;
#22276=CONICAL_SURFACE ( 'NONE', #5792, 3.047499999999988329, 1.047197551196594523 ) ;
#22375=AXIS2_PLACEMENT_3D ( 'NONE', #17535, #9236, #16288 ) ;
#22409=ORIENTED_EDGE ( 'NONE', *, *, #4970, .F. ) ;
#22447=CARTESIAN_POINT ( 'NONE',  ( -10.85980368455889433, 163.6991139211620236, 126.9796742121690443 ) ) ;
#22465=CARTESIAN_POINT ( 'NONE',  ( -17.35589273022797485, 113.6997816401180472, 127.3226006773067525 ) ) ;
#22556=EDGE_CURVE ( 'NONE', #1880, #17838, #18399, .T. ) ;
#22593=SURFACE_STYLE_USAGE ( .BOTH. , #20899 ) ;
#22604=FACE_OUTER_BOUND ( 'NONE', #7998, .T. ) ;
#22612=EDGE_LOOP ( 'NONE', ( #10843, #6968, #4900, #13969 ) ) ;
#22626=EDGE_CURVE ( 'NONE', #8399, #14240, #16797, .T. ) ;
#22658=CARTESIAN_POINT ( 'NONE',  ( -10.92070568566948197, 73.91464330287723783, 120.9748739040315968 ) ) ;
ENDSEC;
END-ISO-10303-21;
